ISO-10303-21;
HEADER;
/* Generated by software containing ST-Developer
 * from STEP Tools, Inc. (www.steptools.com) 
 */

FILE_DESCRIPTION(
/* description */ ('PAT-015'),
/* implementation_level */ '2;1');

FILE_NAME(
/* name */ 'Adjuster knob.step',
/* time_stamp */ '2026-10-29T16:03:43-07:00',
/* author */ (''),
/* organization */ (''),
/* preprocessor_version */ 'ST-DEVELOPER v20.2',
/* originating_system */ 'Autodesk Translation Framework v15.17.0.0',
/* authorisation */ '');

FILE_SCHEMA (('AUTOMOTIVE_DESIGN { 1 0 10303 214 3 1 1 }'));
ENDSEC;

DATA;
#10=MECHANICAL_DESIGN_GEOMETRIC_PRESENTATION_REPRESENTATION('',(#247),#10266);
#199=SHAPE_REPRESENTATION_RELATIONSHIP('SRR','None',#10370,#222);
#222=ADVANCED_BREP_SHAPE_REPRESENTATION('',(#272),#10258);
#247=STYLED_ITEM('',(#10533),#272);
#272=MANIFOLD_SOLID_BREP('Body1',#4706);
#407=FACE_BOUND('',#1180,.T.);
#408=FACE_BOUND('',#1182,.T.);
#409=FACE_BOUND('',#1184,.T.);
#410=FACE_BOUND('',#1186,.T.);
#520=PLANE('',#5399);
#521=PLANE('',#5404);
#522=PLANE('',#5411);
#523=PLANE('',#5412);
#778=FACE_OUTER_BOUND('',#1176,.T.);
#779=FACE_OUTER_BOUND('',#1177,.T.);
#780=FACE_OUTER_BOUND('',#1178,.T.);
#781=FACE_OUTER_BOUND('',#1179,.T.);
#782=FACE_OUTER_BOUND('',#1181,.T.);
#783=FACE_OUTER_BOUND('',#1183,.T.);
#784=FACE_OUTER_BOUND('',#1185,.T.);
#1176=EDGE_LOOP('',(#3987,#3988,#3989));
#1177=EDGE_LOOP('',(#3990,#3991,#3992,#3993,#3994,#3995,#3996,#3997));
#1178=EDGE_LOOP('',(#3998,#3999));
#1179=EDGE_LOOP('',(#4000,#4001,#4002,#4003));
#1180=EDGE_LOOP('',(#4004,#4005,#4006,#4007));
#1181=EDGE_LOOP('',(#4008,#4009,#4010,#4011));
#1182=EDGE_LOOP('',(#4012));
#1183=EDGE_LOOP('',(#4013));
#1184=EDGE_LOOP('',(#4014));
#1185=EDGE_LOOP('',(#4015));
#1186=EDGE_LOOP('',(#4016));
#1320=B_SPLINE_CURVE_WITH_KNOTS('',3,(#9784,#9785,#9786,#9787,#9788,#9789,
#9790,#9791,#9792,#9793),.UNSPECIFIED.,.F.,.F.,(4,2,2,2,4),(0.665271585430993,
0.692803751398642,0.755746158887619,0.818688566376595,0.846220732344244),
 .UNSPECIFIED.);
#1321=B_SPLINE_CURVE_WITH_KNOTS('',3,(#9796,#9797,#9798,#9799,#9800,#9801,
#9802,#9803,#9804,#9805),.UNSPECIFIED.,.F.,.F.,(4,2,2,2,4),(0.161440812839248,
0.188972978806896,0.251915386295873,0.314857793784849,0.342389959752498),
 .UNSPECIFIED.);
#1322=B_SPLINE_CURVE_WITH_KNOTS('',3,(#9808,#9809,#9810,#9811,#9812,#9813,
#9814,#9815,#9816,#9817,#9818,#9819,#9820,#9821,#9822,#9823,#9824,#9825,
#9826,#9827,#9828,#9829,#9830,#9831,#9832,#9833,#9834,#9835,#9836,#9837,
#9838,#9839,#9840,#9841),.UNSPECIFIED.,.T.,.F.,(4,2,2,2,2,2,2,2,2,2,2,2,
2,2,2,2,4),(0.,0.0622075173149514,0.124415034629903,0.186622241324509,0.248829448019115,
0.311036654713721,0.373243861408326,0.435451378723278,0.497658896038229,
0.559866413353181,0.622073930668132,0.684281137362738,0.746488344057344,
0.80869555075195,0.870902757446556,0.933110274761507,0.995317792076459),
 .UNSPECIFIED.);
#1505=LINE('',#9778,#1785);
#1506=LINE('',#9807,#1786);
#1507=LINE('',#9843,#1787);
#1508=LINE('',#9848,#1788);
#1509=LINE('',#9854,#1789);
#1785=VECTOR('',#6598,1.);
#1786=VECTOR('',#6607,0.165);
#1787=VECTOR('',#6610,1.);
#1788=VECTOR('',#6615,0.4);
#1789=VECTOR('',#6622,1.5);
#2075=CIRCLE('',#5400,0.165);
#2076=CIRCLE('',#5401,0.165);
#2077=CIRCLE('',#5403,0.165);
#2078=CIRCLE('',#5406,0.4);
#2079=CIRCLE('',#5407,0.4);
#2080=CIRCLE('',#5409,1.5);
#2081=CIRCLE('',#5410,1.5);
#2409=VERTEX_POINT('',#9776);
#2410=VERTEX_POINT('',#9777);
#2411=VERTEX_POINT('',#9779);
#2412=VERTEX_POINT('',#9783);
#2413=VERTEX_POINT('',#9794);
#2414=VERTEX_POINT('',#9806);
#2415=VERTEX_POINT('',#9845);
#2416=VERTEX_POINT('',#9847);
#2417=VERTEX_POINT('',#9851);
#2418=VERTEX_POINT('',#9853);
#2949=EDGE_CURVE('',#2409,#2410,#1505,.T.);
#2950=EDGE_CURVE('',#2409,#2411,#2075,.T.);
#2951=EDGE_CURVE('',#2411,#2410,#2076,.T.);
#2952=EDGE_CURVE('',#2412,#2409,#1320,.T.);
#2953=EDGE_CURVE('',#2413,#2412,#2077,.T.);
#2954=EDGE_CURVE('',#2410,#2413,#1321,.T.);
#2955=EDGE_CURVE('',#2411,#2414,#1506,.T.);
#2956=EDGE_CURVE('',#2414,#2414,#1322,.T.);
#2957=EDGE_CURVE('',#2413,#2412,#1507,.T.);
#2958=EDGE_CURVE('',#2415,#2415,#2078,.T.);
#2959=EDGE_CURVE('',#2415,#2416,#1508,.T.);
#2960=EDGE_CURVE('',#2416,#2416,#2079,.T.);
#2961=EDGE_CURVE('',#2417,#2417,#2080,.T.);
#2962=EDGE_CURVE('',#2417,#2418,#1509,.T.);
#2963=EDGE_CURVE('',#2418,#2418,#2081,.T.);
#3987=ORIENTED_EDGE('',*,*,#2949,.F.);
#3988=ORIENTED_EDGE('',*,*,#2950,.T.);
#3989=ORIENTED_EDGE('',*,*,#2951,.T.);
#3990=ORIENTED_EDGE('',*,*,#2952,.F.);
#3991=ORIENTED_EDGE('',*,*,#2953,.F.);
#3992=ORIENTED_EDGE('',*,*,#2954,.F.);
#3993=ORIENTED_EDGE('',*,*,#2951,.F.);
#3994=ORIENTED_EDGE('',*,*,#2955,.T.);
#3995=ORIENTED_EDGE('',*,*,#2956,.F.);
#3996=ORIENTED_EDGE('',*,*,#2955,.F.);
#3997=ORIENTED_EDGE('',*,*,#2950,.F.);
#3998=ORIENTED_EDGE('',*,*,#2957,.F.);
#3999=ORIENTED_EDGE('',*,*,#2953,.T.);
#4000=ORIENTED_EDGE('',*,*,#2958,.F.);
#4001=ORIENTED_EDGE('',*,*,#2959,.T.);
#4002=ORIENTED_EDGE('',*,*,#2960,.T.);
#4003=ORIENTED_EDGE('',*,*,#2959,.F.);
#4004=ORIENTED_EDGE('',*,*,#2954,.T.);
#4005=ORIENTED_EDGE('',*,*,#2957,.T.);
#4006=ORIENTED_EDGE('',*,*,#2952,.T.);
#4007=ORIENTED_EDGE('',*,*,#2949,.T.);
#4008=ORIENTED_EDGE('',*,*,#2961,.F.);
#4009=ORIENTED_EDGE('',*,*,#2962,.T.);
#4010=ORIENTED_EDGE('',*,*,#2963,.T.);
#4011=ORIENTED_EDGE('',*,*,#2962,.F.);
#4012=ORIENTED_EDGE('',*,*,#2956,.T.);
#4013=ORIENTED_EDGE('',*,*,#2961,.T.);
#4014=ORIENTED_EDGE('',*,*,#2958,.T.);
#4015=ORIENTED_EDGE('',*,*,#2963,.F.);
#4016=ORIENTED_EDGE('',*,*,#2960,.F.);
#4394=CYLINDRICAL_SURFACE('',#5402,0.165);
#4395=CYLINDRICAL_SURFACE('',#5405,0.4);
#4396=CYLINDRICAL_SURFACE('',#5408,1.5);
#4613=ADVANCED_FACE('',(#778),#520,.T.);
#4614=ADVANCED_FACE('',(#779),#4394,.F.);
#4615=ADVANCED_FACE('',(#780),#521,.T.);
#4616=ADVANCED_FACE('',(#781,#407),#4395,.F.);
#4617=ADVANCED_FACE('',(#782,#408),#4396,.T.);
#4618=ADVANCED_FACE('',(#783,#409),#522,.T.);
#4619=ADVANCED_FACE('',(#784,#410),#523,.F.);
#4706=CLOSED_SHELL('',(#4613,#4614,#4615,#4616,#4617,#4618,#4619));
#5398=AXIS2_PLACEMENT_3D('',#9774,#6594,#6595);
#5399=AXIS2_PLACEMENT_3D('',#9775,#6596,#6597);
#5400=AXIS2_PLACEMENT_3D('',#9780,#6599,#6600);
#5401=AXIS2_PLACEMENT_3D('',#9781,#6601,#6602);
#5402=AXIS2_PLACEMENT_3D('',#9782,#6603,#6604);
#5403=AXIS2_PLACEMENT_3D('',#9795,#6605,#6606);
#5404=AXIS2_PLACEMENT_3D('',#9842,#6608,#6609);
#5405=AXIS2_PLACEMENT_3D('',#9844,#6611,#6612);
#5406=AXIS2_PLACEMENT_3D('',#9846,#6613,#6614);
#5407=AXIS2_PLACEMENT_3D('',#9849,#6616,#6617);
#5408=AXIS2_PLACEMENT_3D('',#9850,#6618,#6619);
#5409=AXIS2_PLACEMENT_3D('',#9852,#6620,#6621);
#5410=AXIS2_PLACEMENT_3D('',#9855,#6623,#6624);
#5411=AXIS2_PLACEMENT_3D('',#9856,#6625,#6626);
#5412=AXIS2_PLACEMENT_3D('',#9857,#6627,#6628);
#6594=DIRECTION('axis',(0.,0.,1.));
#6595=DIRECTION('refdir',(1.,0.,0.));
#6596=DIRECTION('center_axis',(0.,1.,0.));
#6597=DIRECTION('ref_axis',(1.,0.,0.));
#6598=DIRECTION('',(0.,0.,1.));
#6599=DIRECTION('center_axis',(0.,1.,0.));
#6600=DIRECTION('ref_axis',(1.,0.,0.));
#6601=DIRECTION('center_axis',(0.,1.,0.));
#6602=DIRECTION('ref_axis',(1.,0.,0.));
#6603=DIRECTION('center_axis',(0.,1.,0.));
#6604=DIRECTION('ref_axis',(1.,0.,0.));
#6605=DIRECTION('center_axis',(0.,1.,0.));
#6606=DIRECTION('ref_axis',(1.,0.,0.));
#6607=DIRECTION('',(0.,1.,0.));
#6608=DIRECTION('center_axis',(0.,1.,0.));
#6609=DIRECTION('ref_axis',(1.,0.,0.));
#6610=DIRECTION('',(0.,0.,-1.));
#6611=DIRECTION('center_axis',(0.,0.,1.));
#6612=DIRECTION('ref_axis',(1.,0.,0.));
#6613=DIRECTION('center_axis',(0.,0.,-1.));
#6614=DIRECTION('ref_axis',(1.,0.,0.));
#6615=DIRECTION('',(0.,0.,-1.));
#6616=DIRECTION('center_axis',(0.,0.,-1.));
#6617=DIRECTION('ref_axis',(1.,0.,0.));
#6618=DIRECTION('center_axis',(0.,0.,1.));
#6619=DIRECTION('ref_axis',(1.,0.,0.));
#6620=DIRECTION('center_axis',(0.,0.,1.));
#6621=DIRECTION('ref_axis',(1.,0.,0.));
#6622=DIRECTION('',(0.,0.,-1.));
#6623=DIRECTION('center_axis',(0.,0.,1.));
#6624=DIRECTION('ref_axis',(1.,0.,0.));
#6625=DIRECTION('center_axis',(0.,0.,1.));
#6626=DIRECTION('ref_axis',(1.,0.,0.));
#6627=DIRECTION('center_axis',(0.,0.,1.));
#6628=DIRECTION('ref_axis',(1.,0.,0.));
#9774=CARTESIAN_POINT('',(0.,0.,0.));
#9775=CARTESIAN_POINT('Origin',(0.,0.39,11.));
#9776=CARTESIAN_POINT('',(-0.088881944173156,0.39,10.8609856122554));
#9777=CARTESIAN_POINT('',(-0.088881944173156,0.39,11.1390143877446));
#9778=CARTESIAN_POINT('',(-0.088881944173156,0.39,10.5));
#9779=CARTESIAN_POINT('',(-0.165,0.39,11.));
#9780=CARTESIAN_POINT('Origin',(0.,0.39,11.));
#9781=CARTESIAN_POINT('Origin',(0.,0.39,11.));
#9782=CARTESIAN_POINT('Origin',(0.,0.39,11.));
#9783=CARTESIAN_POINT('',(0.088881944173156,0.39,10.8609856122554));
#9784=CARTESIAN_POINT('Ctrl Pts',(0.088881944173156,0.39,10.8609856122554));
#9785=CARTESIAN_POINT('Ctrl Pts',(0.0808964434200154,0.391819914954193,
10.8558799045395));
#9786=CARTESIAN_POINT('Ctrl Pts',(0.072364333302368,0.393502517883282,10.8514036081398));
#9787=CARTESIAN_POINT('Ctrl Pts',(0.0431949313468624,0.398191715532106,
10.8392437758303));
#9788=CARTESIAN_POINT('Ctrl Pts',(0.0209808024963256,0.4,10.835));
#9789=CARTESIAN_POINT('Ctrl Pts',(-0.0209808024963256,0.4,10.835));
#9790=CARTESIAN_POINT('Ctrl Pts',(-0.0431949313468624,0.398191715532106,
10.8392437758303));
#9791=CARTESIAN_POINT('Ctrl Pts',(-0.072364333302368,0.393502517883282,
10.8514036081398));
#9792=CARTESIAN_POINT('Ctrl Pts',(-0.0808964434200154,0.391819914954193,
10.8558799045395));
#9793=CARTESIAN_POINT('Ctrl Pts',(-0.088881944173156,0.39,10.8609856122554));
#9794=CARTESIAN_POINT('',(0.088881944173156,0.39,11.1390143877446));
#9795=CARTESIAN_POINT('Origin',(0.,0.39,11.));
#9796=CARTESIAN_POINT('Ctrl Pts',(-0.088881944173156,0.39,11.1390143877446));
#9797=CARTESIAN_POINT('Ctrl Pts',(-0.0808964434200154,0.391819914954193,
11.1441200954605));
#9798=CARTESIAN_POINT('Ctrl Pts',(-0.072364333302368,0.393502517883282,
11.1485963918602));
#9799=CARTESIAN_POINT('Ctrl Pts',(-0.0431949313468623,0.398191715532106,
11.1607562241697));
#9800=CARTESIAN_POINT('Ctrl Pts',(-0.0209808024963255,0.4,11.165));
#9801=CARTESIAN_POINT('Ctrl Pts',(0.0209808024963256,0.4,11.165));
#9802=CARTESIAN_POINT('Ctrl Pts',(0.0431949313468623,0.398191715532106,
11.1607562241697));
#9803=CARTESIAN_POINT('Ctrl Pts',(0.072364333302368,0.393502517883282,11.1485963918602));
#9804=CARTESIAN_POINT('Ctrl Pts',(0.0808964434200153,0.391819914954193,
11.1441200954605));
#9805=CARTESIAN_POINT('Ctrl Pts',(0.088881944173156,0.39,11.1390143877446));
#9806=CARTESIAN_POINT('',(-0.165,1.49089738077441,11.));
#9807=CARTESIAN_POINT('',(-0.165,0.39,11.));
#9808=CARTESIAN_POINT('Ctrl Pts',(-0.165,1.49089738077441,11.));
#9809=CARTESIAN_POINT('Ctrl Pts',(-0.165,1.49089738077441,10.979264160895));
#9810=CARTESIAN_POINT('Ctrl Pts',(-0.160852499025073,1.49137458218466,10.9571577290991));
#9811=CARTESIAN_POINT('Ctrl Pts',(-0.144008447160944,1.49309518705251,10.916510155069));
#9812=CARTESIAN_POINT('Ctrl Pts',(-0.131312810193433,1.49431341615515,10.8979675724019));
#9813=CARTESIAN_POINT('Ctrl Pts',(-0.102032500700889,1.49659781052539,10.8686872629093));
#9814=CARTESIAN_POINT('Ctrl Pts',(-0.0834898860986569,1.49781281581157,
10.8559915687804));
#9815=CARTESIAN_POINT('Ctrl Pts',(-0.042842204593242,1.49952603771524,10.8391474746158));
#9816=CARTESIAN_POINT('Ctrl Pts',(-0.0207357355648686,1.5,10.835));
#9817=CARTESIAN_POINT('Ctrl Pts',(0.0207357355648686,1.5,10.835));
#9818=CARTESIAN_POINT('Ctrl Pts',(0.0428422045932419,1.49952603771524,10.8391474746158));
#9819=CARTESIAN_POINT('Ctrl Pts',(0.0834898860986569,1.49781281581157,10.8559915687804));
#9820=CARTESIAN_POINT('Ctrl Pts',(0.102032500700889,1.49659781052539,10.8686872629093));
#9821=CARTESIAN_POINT('Ctrl Pts',(0.131312810193433,1.49431341615515,10.8979675724019));
#9822=CARTESIAN_POINT('Ctrl Pts',(0.144008447160944,1.49309518705251,10.916510155069));
#9823=CARTESIAN_POINT('Ctrl Pts',(0.160852499025073,1.49137458218466,10.9571577290991));
#9824=CARTESIAN_POINT('Ctrl Pts',(0.165,1.49089738077441,10.979264160895));
#9825=CARTESIAN_POINT('Ctrl Pts',(0.165,1.49089738077441,11.020735839105));
#9826=CARTESIAN_POINT('Ctrl Pts',(0.160852499025073,1.49137458218466,11.0428422709009));
#9827=CARTESIAN_POINT('Ctrl Pts',(0.144008447160944,1.49309518705251,11.083489844931));
#9828=CARTESIAN_POINT('Ctrl Pts',(0.131312810193433,1.49431341615515,11.1020324275981));
#9829=CARTESIAN_POINT('Ctrl Pts',(0.102032500700889,1.49659781052539,11.1313127370907));
#9830=CARTESIAN_POINT('Ctrl Pts',(0.0834898860986569,1.49781281581157,11.1440084312196));
#9831=CARTESIAN_POINT('Ctrl Pts',(0.042842204593242,1.49952603771524,11.1608525253842));
#9832=CARTESIAN_POINT('Ctrl Pts',(0.0207357355648686,1.5,11.165));
#9833=CARTESIAN_POINT('Ctrl Pts',(-0.0207357355648686,1.5,11.165));
#9834=CARTESIAN_POINT('Ctrl Pts',(-0.0428422045932419,1.49952603771524,
11.1608525253842));
#9835=CARTESIAN_POINT('Ctrl Pts',(-0.0834898860986569,1.49781281581157,
11.1440084312196));
#9836=CARTESIAN_POINT('Ctrl Pts',(-0.102032500700889,1.49659781052539,11.1313127370907));
#9837=CARTESIAN_POINT('Ctrl Pts',(-0.131312810193433,1.49431341615515,11.1020324275981));
#9838=CARTESIAN_POINT('Ctrl Pts',(-0.144008447160944,1.49309518705251,11.083489844931));
#9839=CARTESIAN_POINT('Ctrl Pts',(-0.160852499025073,1.49137458218466,11.0428422709009));
#9840=CARTESIAN_POINT('Ctrl Pts',(-0.165,1.49089738077441,11.020735839105));
#9841=CARTESIAN_POINT('Ctrl Pts',(-0.165,1.49089738077441,11.));
#9842=CARTESIAN_POINT('Origin',(0.,0.39,11.));
#9843=CARTESIAN_POINT('',(0.088881944173156,0.39,10.5));
#9844=CARTESIAN_POINT('Origin',(0.,0.,10.5));
#9845=CARTESIAN_POINT('',(-0.4,-4.89858719658941E-17,11.5));
#9846=CARTESIAN_POINT('Origin',(0.,0.,11.5));
#9847=CARTESIAN_POINT('',(-0.4,-4.89858719658941E-17,10.5));
#9848=CARTESIAN_POINT('',(-0.4,-4.89858719658941E-17,10.5));
#9849=CARTESIAN_POINT('Origin',(0.,0.,10.5));
#9850=CARTESIAN_POINT('Origin',(0.,0.,10.5));
#9851=CARTESIAN_POINT('',(-1.5,-1.83697019872103E-16,11.5));
#9852=CARTESIAN_POINT('Origin',(0.,0.,11.5));
#9853=CARTESIAN_POINT('',(-1.5,-1.83697019872103E-16,10.5));
#9854=CARTESIAN_POINT('',(-1.5,-1.83697019872103E-16,10.5));
#9855=CARTESIAN_POINT('Origin',(0.,0.,10.5));
#9856=CARTESIAN_POINT('Origin',(0.,0.,11.5));
#9857=CARTESIAN_POINT('Origin',(0.,0.,10.5));
#10233=UNCERTAINTY_MEASURE_WITH_UNIT(LENGTH_MEASURE(0.001),#10267,
'DISTANCE_ACCURACY_VALUE',
'Maximum model space distance between geometric entities at asserted c
onnectivities');
#10241=UNCERTAINTY_MEASURE_WITH_UNIT(LENGTH_MEASURE(0.001),#10267,
'DISTANCE_ACCURACY_VALUE',
'Maximum model space distance between geometric entities at asserted c
onnectivities');
#10258=(
GEOMETRIC_REPRESENTATION_CONTEXT(3)
GLOBAL_UNCERTAINTY_ASSIGNED_CONTEXT((#10233))
GLOBAL_UNIT_ASSIGNED_CONTEXT((#10267,#10269,#10270))
REPRESENTATION_CONTEXT('','3D')
);
#10266=(
GEOMETRIC_REPRESENTATION_CONTEXT(3)
GLOBAL_UNCERTAINTY_ASSIGNED_CONTEXT((#10241))
GLOBAL_UNIT_ASSIGNED_CONTEXT((#10267,#10269,#10270))
REPRESENTATION_CONTEXT('','3D')
);
#10267=(
LENGTH_UNIT()
NAMED_UNIT(*)
SI_UNIT(.CENTI.,.METRE.)
);
#10269=(
NAMED_UNIT(*)
PLANE_ANGLE_UNIT()
SI_UNIT($,.RADIAN.)
);
#10270=(
NAMED_UNIT(*)
SI_UNIT($,.STERADIAN.)
SOLID_ANGLE_UNIT()
);
#10287=SHAPE_DEFINITION_REPRESENTATION(#10311,#10370);
#10311=PRODUCT_DEFINITION_SHAPE('',$,#10395);
#10370=SHAPE_REPRESENTATION('',(#5398),#10258);
#10378=PRODUCT_DEFINITION_CONTEXT('part definition',#10452,'design');
#10395=PRODUCT_DEFINITION('Adjuster knob','Adjuster knob',#10419,
#10378);
#10419=PRODUCT_DEFINITION_FORMATION('',$,#10470);
#10452=APPLICATION_CONTEXT(
'Core Data for Automotive Mechanical Design Process');
#10453=PRODUCT_CONTEXT('part definition',#10452,'mechanical');
#10470=PRODUCT('Adjuster knob','Adjuster knob',
'Adjuster knob',(#10453));
#10527=COLOUR_RGB('Light Blue',0.38,0.62,0.78);
#10528=FILL_AREA_STYLE_COLOUR('',#10527);
#10529=FILL_AREA_STYLE('',(#10528));
#10530=SURFACE_STYLE_FILL_AREA(#10529);
#10531=SURFACE_SIDE_STYLE('',(#10530));
#10532=SURFACE_STYLE_USAGE(.BOTH.,#10531);
#10533=PRESENTATION_STYLE_ASSIGNMENT((#10532));
ENDSEC;
END-ISO-10303-21;
